ISO-10303-21;
HEADER;
/* Generated by software containing ST-Developer
 * from STEP Tools, Inc. (www.steptools.com) 
 */

FILE_DESCRIPTION(
/* description */ ('Bin tilter linkage'),
/* implementation_level */ '2;1');

FILE_NAME(
/* name */ 'Screw keeper fastener (6).step',
/* time_stamp */ '2026-10-28T03:26:24-07:00',
/* author */ (''),
/* organization */ (''),
/* preprocessor_version */ 'ST-DEVELOPER v20.2',
/* originating_system */ 'Autodesk Translation Framework v15.17.0.0',
/* authorisation */ '');

FILE_SCHEMA (('AUTOMOTIVE_DESIGN { 1 0 10303 214 3 1 1 }'));
ENDSEC;

DATA;
#10=MECHANICAL_DESIGN_GEOMETRIC_PRESENTATION_REPRESENTATION('',(#887),#23728);
#675=SHAPE_REPRESENTATION_RELATIONSHIP('SRR','None',#24139,#781);
#781=ADVANCED_BREP_SHAPE_REPRESENTATION('',(#1001),#23639);
#887=STYLED_ITEM('',(#24772),#1001);
#1001=MANIFOLD_SOLID_BREP('Body1',#12417);
#1231=FACE_BOUND('',#3028,.T.);
#1596=PLANE('',#14144);
#1597=PLANE('',#14149);
#1598=PLANE('',#14152);
#2106=FACE_OUTER_BOUND('',#3027,.T.);
#2107=FACE_OUTER_BOUND('',#3029,.T.);
#2108=FACE_OUTER_BOUND('',#3030,.T.);
#2109=FACE_OUTER_BOUND('',#3031,.T.);
#2110=FACE_OUTER_BOUND('',#3032,.T.);
#3027=EDGE_LOOP('',(#9273));
#3028=EDGE_LOOP('',(#9274));
#3029=EDGE_LOOP('',(#9275,#9276,#9277,#9278));
#3030=EDGE_LOOP('',(#9279));
#3031=EDGE_LOOP('',(#9280,#9281,#9282,#9283));
#3032=EDGE_LOOP('',(#9284));
#4075=LINE('',#20747,#4750);
#4076=LINE('',#20751,#4751);
#4750=VECTOR('',#16646,0.35);
#4751=VECTOR('',#16651,0.199999999999999);
#5423=CIRCLE('',#14145,0.35);
#5424=CIRCLE('',#14146,0.199999999999999);
#5425=CIRCLE('',#14148,0.35);
#5426=CIRCLE('',#14151,0.199999999999999);
#6257=VERTEX_POINT('',#20740);
#6258=VERTEX_POINT('',#20742);
#6259=VERTEX_POINT('',#20745);
#6260=VERTEX_POINT('',#20750);
#7376=EDGE_CURVE('',#6257,#6257,#5423,.T.);
#7377=EDGE_CURVE('',#6258,#6258,#5424,.T.);
#7378=EDGE_CURVE('',#6259,#6259,#5425,.T.);
#7379=EDGE_CURVE('',#6259,#6257,#4075,.T.);
#7380=EDGE_CURVE('',#6258,#6260,#4076,.T.);
#7381=EDGE_CURVE('',#6260,#6260,#5426,.T.);
#9273=ORIENTED_EDGE('',*,*,#7376,.F.);
#9274=ORIENTED_EDGE('',*,*,#7377,.T.);
#9275=ORIENTED_EDGE('',*,*,#7378,.F.);
#9276=ORIENTED_EDGE('',*,*,#7379,.T.);
#9277=ORIENTED_EDGE('',*,*,#7376,.T.);
#9278=ORIENTED_EDGE('',*,*,#7379,.F.);
#9279=ORIENTED_EDGE('',*,*,#7378,.T.);
#9280=ORIENTED_EDGE('',*,*,#7377,.F.);
#9281=ORIENTED_EDGE('',*,*,#7380,.T.);
#9282=ORIENTED_EDGE('',*,*,#7381,.T.);
#9283=ORIENTED_EDGE('',*,*,#7380,.F.);
#9284=ORIENTED_EDGE('',*,*,#7381,.F.);
#11379=CYLINDRICAL_SURFACE('',#14147,0.35);
#11380=CYLINDRICAL_SURFACE('',#14150,0.199999999999999);
#11831=ADVANCED_FACE('',(#2106,#1231),#1596,.F.);
#11832=ADVANCED_FACE('',(#2107),#11379,.T.);
#11833=ADVANCED_FACE('',(#2108),#1597,.T.);
#11834=ADVANCED_FACE('',(#2109),#11380,.T.);
#11835=ADVANCED_FACE('',(#2110),#1598,.F.);
#12417=CLOSED_SHELL('',(#11831,#11832,#11833,#11834,#11835));
#14143=AXIS2_PLACEMENT_3D('',#20738,#16634,#16635);
#14144=AXIS2_PLACEMENT_3D('',#20739,#16636,#16637);
#14145=AXIS2_PLACEMENT_3D('',#20741,#16638,#16639);
#14146=AXIS2_PLACEMENT_3D('',#20743,#16640,#16641);
#14147=AXIS2_PLACEMENT_3D('',#20744,#16642,#16643);
#14148=AXIS2_PLACEMENT_3D('',#20746,#16644,#16645);
#14149=AXIS2_PLACEMENT_3D('',#20748,#16647,#16648);
#14150=AXIS2_PLACEMENT_3D('',#20749,#16649,#16650);
#14151=AXIS2_PLACEMENT_3D('',#20752,#16652,#16653);
#14152=AXIS2_PLACEMENT_3D('',#20753,#16654,#16655);
#16634=DIRECTION('axis',(0.,0.,1.));
#16635=DIRECTION('refdir',(1.,0.,0.));
#16636=DIRECTION('center_axis',(1.,0.,0.));
#16637=DIRECTION('ref_axis',(0.,0.,-1.));
#16638=DIRECTION('center_axis',(1.,0.,0.));
#16639=DIRECTION('ref_axis',(0.,0.,-1.));
#16640=DIRECTION('center_axis',(1.,0.,0.));
#16641=DIRECTION('ref_axis',(0.,0.,-1.));
#16642=DIRECTION('center_axis',(1.,0.,0.));
#16643=DIRECTION('ref_axis',(0.,0.,-1.));
#16644=DIRECTION('center_axis',(1.,0.,0.));
#16645=DIRECTION('ref_axis',(0.,0.,-1.));
#16646=DIRECTION('',(-1.,0.,0.));
#16647=DIRECTION('center_axis',(1.,0.,0.));
#16648=DIRECTION('ref_axis',(0.,0.,-1.));
#16649=DIRECTION('center_axis',(1.,0.,0.));
#16650=DIRECTION('ref_axis',(0.,0.,-1.));
#16651=DIRECTION('',(-1.,0.,0.));
#16652=DIRECTION('center_axis',(1.,0.,0.));
#16653=DIRECTION('ref_axis',(0.,0.,-1.));
#16654=DIRECTION('center_axis',(1.,0.,0.));
#16655=DIRECTION('ref_axis',(0.,0.,-1.));
#20738=CARTESIAN_POINT('',(0.,0.,0.));
#20739=CARTESIAN_POINT('Origin',(1.2,-4.5,9.85));
#20740=CARTESIAN_POINT('',(1.2,-4.5,10.2));
#20741=CARTESIAN_POINT('Origin',(1.2,-4.5,9.85));
#20742=CARTESIAN_POINT('',(1.2,-4.5,10.05));
#20743=CARTESIAN_POINT('Origin',(1.2,-4.5,9.85));
#20744=CARTESIAN_POINT('Origin',(1.2,-4.5,9.85));
#20745=CARTESIAN_POINT('',(1.6,-4.5,10.2));
#20746=CARTESIAN_POINT('Origin',(1.6,-4.5,9.85));
#20747=CARTESIAN_POINT('',(1.2,-4.5,10.2));
#20748=CARTESIAN_POINT('Origin',(1.6,-4.5,9.85));
#20749=CARTESIAN_POINT('Origin',(0.5,-4.5,9.85));
#20750=CARTESIAN_POINT('',(0.5,-4.5,10.05));
#20751=CARTESIAN_POINT('',(0.5,-4.5,10.05));
#20752=CARTESIAN_POINT('Origin',(0.5,-4.5,9.85));
#20753=CARTESIAN_POINT('Origin',(0.5,-4.5,9.85));
#23522=UNCERTAINTY_MEASURE_WITH_UNIT(LENGTH_MEASURE(0.001),#23729,
'DISTANCE_ACCURACY_VALUE',
'Maximum model space distance between geometric entities at asserted c
onnectivities');
#23611=UNCERTAINTY_MEASURE_WITH_UNIT(LENGTH_MEASURE(0.001),#23729,
'DISTANCE_ACCURACY_VALUE',
'Maximum model space distance between geometric entities at asserted c
onnectivities');
#23639=(
GEOMETRIC_REPRESENTATION_CONTEXT(3)
GLOBAL_UNCERTAINTY_ASSIGNED_CONTEXT((#23522))
GLOBAL_UNIT_ASSIGNED_CONTEXT((#23729,#23731,#23732))
REPRESENTATION_CONTEXT('','3D')
);
#23728=(
GEOMETRIC_REPRESENTATION_CONTEXT(3)
GLOBAL_UNCERTAINTY_ASSIGNED_CONTEXT((#23611))
GLOBAL_UNIT_ASSIGNED_CONTEXT((#23729,#23731,#23732))
REPRESENTATION_CONTEXT('','3D')
);
#23729=(
LENGTH_UNIT()
NAMED_UNIT(*)
SI_UNIT(.CENTI.,.METRE.)
);
#23731=(
NAMED_UNIT(*)
PLANE_ANGLE_UNIT()
SI_UNIT($,.RADIAN.)
);
#23732=(
NAMED_UNIT(*)
SI_UNIT($,.STERADIAN.)
SOLID_ANGLE_UNIT()
);
#23760=SHAPE_DEFINITION_REPRESENTATION(#23876,#24139);
#23876=PRODUCT_DEFINITION_SHAPE('',$,#24256);
#24139=SHAPE_REPRESENTATION('',(#14143),#23639);
#24228=PRODUCT_DEFINITION_CONTEXT('part definition',#24578,'design');
#24256=PRODUCT_DEFINITION('Screw keeper fastener (6)',
'Screw keeper fastener (6)',#24372,#24228);
#24372=PRODUCT_DEFINITION_FORMATION('',$,#24607);
#24578=APPLICATION_CONTEXT(
'Core Data for Automotive Mechanical Design Process');
#24579=PRODUCT_CONTEXT('part definition',#24578,'mechanical');
#24607=PRODUCT('Screw keeper fastener (6)','Screw keeper fastener (6)',
'Screw keeper fastener (6)',(#24579));
#24766=COLOUR_RGB('Black',0.12,0.14,0.17);
#24767=FILL_AREA_STYLE_COLOUR('',#24766);
#24768=FILL_AREA_STYLE('',(#24767));
#24769=SURFACE_STYLE_FILL_AREA(#24768);
#24770=SURFACE_SIDE_STYLE('',(#24769));
#24771=SURFACE_STYLE_USAGE(.BOTH.,#24770);
#24772=PRESENTATION_STYLE_ASSIGNMENT((#24771));
ENDSEC;
END-ISO-10303-21;
